ISO-10303-21;
HEADER;
FILE_DESCRIPTION (('STEP AP214'),
    '1' );
FILE_NAME ('Part 32,6_Varsayılan.step',
    '2026-10-10T17:45:43',
    ( '' ),
    ( '' ),
    'SwSTEP 2.0',
    'SolidWorks 2024',
    '' );
FILE_SCHEMA (( 'AUTOMOTIVE_DESIGN' ));
ENDSEC;

DATA;
#52=EDGE_LOOP ( 'NONE', ( #3560, #240, #914, #1362 ) ) ;
#70=DIRECTION ( 'NONE',  ( 1.000000000000000000, 0.000000000000000000, 0.000000000000000000 ) ) ;
#105=DIRECTION ( 'NONE',  ( 0.000000000000000000, 0.000000000000000000, 1.000000000000000000 ) ) ;
#213=ORIENTED_EDGE ( 'NONE', *, *, #6031, .T. ) ;
#240=ORIENTED_EDGE ( 'NONE', *, *, #3676, .T. ) ;
#248=DIRECTION ( 'NONE',  ( 1.000000000000000000, 0.000000000000000000, 0.000000000000000000 ) ) ;
#290=CARTESIAN_POINT ( 'NONE',  ( 0.000000000000000000, 0.000000000000000000, 0.000000000000000000 ) ) ;
#349=ORIENTED_EDGE ( 'NONE', *, *, #5310, .T. ) ;
#371=VERTEX_POINT ( 'NONE', #5182 ) ;
#480=CARTESIAN_POINT ( 'NONE',  ( 6.500000000000000000, 0.000000000000000000, 1.000000000000000888 ) ) ;
#486=( LENGTH_UNIT ( ) NAMED_UNIT ( * ) SI_UNIT ( .MILLI., .METRE. ) );
#520=TOROIDAL_SURFACE ( 'NONE', #621, 6.500000000000000000, 1.000000000000000000 ) ;
#560=ORIENTED_EDGE ( 'NONE', *, *, #6031, .F. ) ;
#616=DIRECTION ( 'NONE',  ( -0.000000000000000000, -0.000000000000000000, -1.000000000000000000 ) ) ;
#621=AXIS2_PLACEMENT_3D ( 'NONE', #3961, #3985, #4962 ) ;
#650=DIRECTION ( 'NONE',  ( 0.000000000000000000, 0.000000000000000000, 1.000000000000000000 ) ) ;
#661=VERTEX_POINT ( 'NONE', #2983 ) ;
#684=AXIS2_PLACEMENT_3D ( 'NONE', #4760, #4654, #248 ) ;
#714=( NAMED_UNIT ( * ) PLANE_ANGLE_UNIT ( ) SI_UNIT ( $, .RADIAN. ) );
#787=CARTESIAN_POINT ( 'NONE',  ( 6.500000000000000000, 0.000000000000000000, 0.000000000000000000 ) ) ;
#815=ORIENTED_EDGE ( 'NONE', *, *, #5748, .F. ) ;
#819=DIRECTION ( 'NONE',  ( -1.000000000000000000, 1.224646799147352468E-16, 0.000000000000000000 ) ) ;
#846=ORIENTED_EDGE ( 'NONE', *, *, #3676, .F. ) ;
#849=AXIS2_PLACEMENT_3D ( 'NONE', #4076, #1637, #5460 ) ;
#854=ORIENTED_EDGE ( 'NONE', *, *, #1411, .T. ) ;
#873=CARTESIAN_POINT ( 'NONE',  ( -6.500000000000000000, 8.572527594031472204E-16, 0.000000000000000000 ) ) ;
#914=ORIENTED_EDGE ( 'NONE', *, *, #5064, .F. ) ;
#962=DIRECTION ( 'NONE',  ( -0.000000000000000000, -0.000000000000000000, -1.000000000000000000 ) ) ;
#1025=CIRCLE ( 'NONE', #5353, 7.500000000000000000 ) ;
#1027=SHAPE_DEFINITION_REPRESENTATION ( #5088, #5606 ) ;
#1064=ADVANCED_FACE ( 'NONE', ( #1149 ), #3631, .F. ) ;
#1070=VERTEX_POINT ( 'NONE', #2179 ) ;
#1149=FACE_OUTER_BOUND ( 'NONE', #4784, .T. ) ;
#1154=AXIS2_PLACEMENT_3D ( 'NONE', #4809, #4253, #3814 ) ;
#1174=DIRECTION ( 'NONE',  ( -1.000000000000000000, 0.000000000000000000, 0.000000000000000000 ) ) ;
#1200=AXIS2_PLACEMENT_3D ( 'NONE', #4326, #3354, #6329 ) ;
#1217=FACE_OUTER_BOUND ( 'NONE', #4623, .T. ) ;
#1271=ORIENTED_EDGE ( 'NONE', *, *, #5310, .F. ) ;
#1276=EDGE_LOOP ( 'NONE', ( #846, #2073, #5755, #2967 ) ) ;
#1290=AXIS2_PLACEMENT_3D ( 'NONE', #3928, #5410, #5832 ) ;
#1291=CARTESIAN_POINT ( 'NONE',  ( -6.500000000000000000, 7.960204194457795477E-16, 47.00000000000000000 ) ) ;
#1333=ADVANCED_BREP_SHAPE_REPRESENTATION ( '', ( #2488, #6349 ), #1412 ) ;
#1362=ORIENTED_EDGE ( 'NONE', *, *, #4072, .F. ) ;
#1394=CIRCLE ( 'NONE', #6237, 7.500000000000000000 ) ;
#1409=DIRECTION ( 'NONE',  ( 1.000000000000000000, 0.000000000000000000, 0.000000000000000000 ) ) ;
#1411=EDGE_CURVE ( 'NONE', #1070, #5642, #1592, .T. ) ;
#1412=( GEOMETRIC_REPRESENTATION_CONTEXT ( 3 ) GLOBAL_UNCERTAINTY_ASSIGNED_CONTEXT ( ( #3212 ) ) GLOBAL_UNIT_ASSIGNED_CONTEXT ( ( #486, #1870, #4793 ) ) REPRESENTATION_CONTEXT ( 'NONE', 'WORKASPACE' ) );
#1440=LINE ( 'NONE', #3880, #4932 ) ;
#1465=ADVANCED_FACE ( 'NONE', ( #2530 ), #2932, .T. ) ;
#1472=ORIENTED_EDGE ( 'NONE', *, *, #1654, .T. ) ;
#1476=DIRECTION ( 'NONE',  ( 1.000000000000000000, 0.000000000000000000, 0.000000000000000000 ) ) ;
#1479=SHAPE_REPRESENTATION_RELATIONSHIP ( 'NONE' , 'NONE' ,  #5606, #1333 ) ;
#1504=DIRECTION ( 'NONE',  ( 0.000000000000000000, -1.000000000000000000, 0.000000000000000000 ) ) ;
#1513=DIRECTION ( 'NONE',  ( 1.000000000000000000, 0.000000000000000000, 0.000000000000000000 ) ) ;
#1525=ADVANCED_FACE ( 'NONE', ( #1662 ), #6083, .T. ) ;
#1551=CLOSED_SHELL ( 'NONE', ( #4759, #1798, #3501, #1525, #5370, #1064, #1465, #4073 ) ) ;
#1592=CIRCLE ( 'NONE', #1290, 7.500000000000000000 ) ;
#1596=EDGE_CURVE ( 'NONE', #5642, #1070, #4267, .T. ) ;
#1604=DIRECTION ( 'NONE',  ( 0.000000000000000000, -1.000000000000000000, 0.000000000000000000 ) ) ;
#1637=DIRECTION ( 'NONE',  ( 0.000000000000000000, 0.000000000000000000, 1.000000000000000000 ) ) ;
#1639=LINE ( 'NONE', #3602, #5123 ) ;
#1654=EDGE_CURVE ( 'NONE', #5649, #2535, #2718, .T. ) ;
#1662=FACE_OUTER_BOUND ( 'NONE', #6247, .T. ) ;
#1798=ADVANCED_FACE ( 'NONE', ( #2833 ), #4766, .T. ) ;
#1813=AXIS2_PLACEMENT_3D ( 'NONE', #5014, #616, #1174 ) ;
#1870=( NAMED_UNIT ( * ) PLANE_ANGLE_UNIT ( ) SI_UNIT ( $, .RADIAN. ) );
#1924=DIRECTION ( 'NONE',  ( 0.000000000000000000, 0.000000000000000000, 1.000000000000000000 ) ) ;
#1952=ORIENTED_EDGE ( 'NONE', *, *, #1411, .F. ) ;
#1962=DIRECTION ( 'NONE',  ( -0.000000000000000000, -0.000000000000000000, -1.000000000000000000 ) ) ;
#1998=FACE_OUTER_BOUND ( 'NONE', #4911, .T. ) ;
#2018=AXIS2_PLACEMENT_3D ( 'NONE', #5052, #4496, #3110 ) ;
#2019=CARTESIAN_POINT ( 'NONE',  ( 0.000000000000000000, 0.000000000000000000, 47.00000000000000000 ) ) ;
#2041=TOROIDAL_SURFACE ( 'NONE', #2446, 6.500000000000000000, 1.000000000000000000 ) ;
#2059=CARTESIAN_POINT ( 'NONE',  ( 0.000000000000000000, 0.000000000000000000, 1.000000000000000888 ) ) ;
#2062=DIRECTION ( 'NONE',  ( -0.000000000000000000, -0.000000000000000000, -1.000000000000000000 ) ) ;
#2073=ORIENTED_EDGE ( 'NONE', *, *, #1654, .F. ) ;
#2079=DIRECTION ( 'NONE',  ( 1.000000000000000000, 0.000000000000000000, 0.000000000000000000 ) ) ;
#2179=CARTESIAN_POINT ( 'NONE',  ( 7.500000000000000000, 9.184850993605147944E-16, 47.00000000000000000 ) ) ;
#2213=CYLINDRICAL_SURFACE ( 'NONE', #4315, 7.500000000000000000 ) ;
#2224=ORIENTED_EDGE ( 'NONE', *, *, #3409, .T. ) ;
#2242=DIRECTION ( 'NONE',  ( 0.000000000000000000, 0.000000000000000000, 1.000000000000000000 ) ) ;
#2254=DIRECTION ( 'NONE',  ( 1.224646799147353207E-16, 1.000000000000000000, -0.000000000000000000 ) ) ;
#2258=ORIENTED_EDGE ( 'NONE', *, *, #3409, .F. ) ;
#2280=EDGE_CURVE ( 'NONE', #6227, #371, #1394, .T. ) ;
#2368=VERTEX_POINT ( 'NONE', #3540 ) ;
#2430=STYLED_ITEM('',(#6419),#2488);
#2446=AXIS2_PLACEMENT_3D ( 'NONE', #2019, #1924, #1476 ) ;
#2460=ORIENTED_EDGE ( 'NONE', *, *, #1596, .T. ) ;
#2488=MANIFOLD_SOLID_BREP ( 'Fillet1', #1551 ) ;
#2499=EDGE_CURVE ( 'NONE', #2535, #5649, #3250, .T. ) ;
#2530=FACE_OUTER_BOUND ( 'NONE', #1276, .T. ) ;
#2535=VERTEX_POINT ( 'NONE', #873 ) ;
#2558=CARTESIAN_POINT ( 'NONE',  ( 0.000000000000000000, 0.000000000000000000, 1.000000000000000888 ) ) ;
#2567=ORIENTED_EDGE ( 'NONE', *, *, #4871, .F. ) ;
#2668=DIRECTION ( 'NONE',  ( -0.000000000000000000, -0.000000000000000000, -1.000000000000000000 ) ) ;
#2718=CIRCLE ( 'NONE', #3553, 6.500000000000000000 ) ;
#2772=CIRCLE ( 'NONE', #6285, 1.000000000000000000 ) ;
#2833=FACE_OUTER_BOUND ( 'NONE', #52, .T. ) ;
#2874=FACE_OUTER_BOUND ( 'NONE', #4752, .T. ) ;
#2932=TOROIDAL_SURFACE ( 'NONE', #2018, 6.500000000000000000, 1.000000000000000000 ) ;
#2967=ORIENTED_EDGE ( 'NONE', *, *, #2280, .F. ) ;
#2983=CARTESIAN_POINT ( 'NONE',  ( -6.500000000000000000, 8.572527594031472204E-16, 48.00000000000000000 ) ) ;
#3025=PRODUCT_DEFINITION_FORMATION_WITH_SPECIFIED_SOURCE ( 'ANY', '', #3229, .NOT_KNOWN. ) ;
#3092=CARTESIAN_POINT ( 'NONE',  ( 0.000000000000000000, 0.000000000000000000, 48.00000000000000000 ) ) ;
#3110=DIRECTION ( 'NONE',  ( 1.000000000000000000, 0.000000000000000000, 0.000000000000000000 ) ) ;
#3147=( LENGTH_UNIT ( ) NAMED_UNIT ( * ) SI_UNIT ( .MILLI., .METRE. ) );
#3157=CIRCLE ( 'NONE', #6259, 1.000000000000000000 ) ;
#3163=DIRECTION ( 'NONE',  ( -0.000000000000000000, -0.000000000000000000, -1.000000000000000000 ) ) ;
#3212=UNCERTAINTY_MEASURE_WITH_UNIT (LENGTH_MEASURE( 1.000000000000000082E-05 ), #486, 'distance_accuracy_value', 'NONE');
#3229=PRODUCT ( 'Part 32,6_Varsay\X2\0131\X0\lan', 'Part 32,6_Varsay\X2\0131\X0\lan', '', ( #5445 ) ) ;
#3250=CIRCLE ( 'NONE', #5941, 6.500000000000000000 ) ;
#3336=PRODUCT_DEFINITION ( 'UNKNOWN', '', #3025, #5707 ) ;
#3354=DIRECTION ( 'NONE',  ( 0.000000000000000000, 0.000000000000000000, 1.000000000000000000 ) ) ;
#3366=FACE_OUTER_BOUND ( 'NONE', #5366, .T. ) ;
#3409=EDGE_CURVE ( 'NONE', #661, #2368, #5557, .T. ) ;
#3501=ADVANCED_FACE ( 'NONE', ( #1217 ), #2213, .T. ) ;
#3540=CARTESIAN_POINT ( 'NONE',  ( 6.500000000000000000, 0.000000000000000000, 48.00000000000000000 ) ) ;
#3553=AXIS2_PLACEMENT_3D ( 'NONE', #5586, #3163, #5074 ) ;
#3560=ORIENTED_EDGE ( 'NONE', *, *, #2499, .F. ) ;
#3602=CARTESIAN_POINT ( 'NONE',  ( 7.500000000000000000, 9.184850993605147944E-16, 48.00000000000000000 ) ) ;
#3604=DIRECTION ( 'NONE',  ( -1.000000000000000000, 0.000000000000000000, 0.000000000000000000 ) ) ;
#3631=PLANE ( 'NONE',  #849 ) ;
#3659=MECHANICAL_DESIGN_GEOMETRIC_PRESENTATION_REPRESENTATION('',(#2430),#4901);
#3660=( NAMED_UNIT ( * ) SI_UNIT ( $, .STERADIAN. ) SOLID_ANGLE_UNIT ( ) );
#3676=EDGE_CURVE ( 'NONE', #2535, #6227, #2772, .T. ) ;
#3790=AXIS2_PLACEMENT_3D ( 'NONE', #480, #1504, #5895 ) ;
#3814=DIRECTION ( 'NONE',  ( 1.000000000000000000, 0.000000000000000000, 0.000000000000000000 ) ) ;
#3817=DIRECTION ( 'NONE',  ( 0.000000000000000000, 0.000000000000000000, 1.000000000000000000 ) ) ;
#3846=CARTESIAN_POINT ( 'NONE',  ( 0.000000000000000000, 0.000000000000000000, 48.00000000000000000 ) ) ;
#3880=CARTESIAN_POINT ( 'NONE',  ( -7.500000000000000000, 0.000000000000000000, 48.00000000000000000 ) ) ;
#3881=CIRCLE ( 'NONE', #1200, 6.500000000000000000 ) ;
#3928=CARTESIAN_POINT ( 'NONE',  ( 0.000000000000000000, 0.000000000000000000, 47.00000000000000000 ) ) ;
#3961=CARTESIAN_POINT ( 'NONE',  ( 0.000000000000000000, 0.000000000000000000, 47.00000000000000000 ) ) ;
#3980=ORIENTED_EDGE ( 'NONE', *, *, #2280, .T. ) ;
#3983=CARTESIAN_POINT ( 'NONE',  ( -6.500000000000000000, 7.960204194457795477E-16, 1.000000000000000888 ) ) ;
#3985=DIRECTION ( 'NONE',  ( 0.000000000000000000, 0.000000000000000000, 1.000000000000000000 ) ) ;
#4072=EDGE_CURVE ( 'NONE', #5649, #371, #4817, .T. ) ;
#4073=ADVANCED_FACE ( 'NONE', ( #3366 ), #2041, .T. ) ;
#4076=CARTESIAN_POINT ( 'NONE',  ( 0.000000000000000000, 0.000000000000000000, 0.000000000000000000 ) ) ;
#4105=ORIENTED_EDGE ( 'NONE', *, *, #5064, .T. ) ;
#4169=DIRECTION ( 'NONE',  ( 1.000000000000000000, 0.000000000000000000, 0.000000000000000000 ) ) ;
#4187=CIRCLE ( 'NONE', #6150, 1.000000000000000888 ) ;
#4251=ORIENTED_EDGE ( 'NONE', *, *, #5986, .F. ) ;
#4253=DIRECTION ( 'NONE',  ( 0.000000000000000000, 0.000000000000000000, 1.000000000000000000 ) ) ;
#4267=CIRCLE ( 'NONE', #684, 7.500000000000000000 ) ;
#4296=ORIENTED_EDGE ( 'NONE', *, *, #1596, .F. ) ;
#4315=AXIS2_PLACEMENT_3D ( 'NONE', #3092, #2668, #3604 ) ;
#4326=CARTESIAN_POINT ( 'NONE',  ( 0.000000000000000000, 0.000000000000000000, 48.00000000000000000 ) ) ;
#4496=DIRECTION ( 'NONE',  ( 0.000000000000000000, 0.000000000000000000, 1.000000000000000000 ) ) ;
#4520=DIRECTION ( 'NONE',  ( 0.000000000000000000, 0.000000000000000000, 1.000000000000000000 ) ) ;
#4623=EDGE_LOOP ( 'NONE', ( #2460, #5329, #4105, #2567 ) ) ;
#4654=DIRECTION ( 'NONE',  ( -0.000000000000000000, -0.000000000000000000, -1.000000000000000000 ) ) ;
#4752=EDGE_LOOP ( 'NONE', ( #349, #2224 ) ) ;
#4759=ADVANCED_FACE ( 'NONE', ( #1998 ), #520, .T. ) ;
#4760=CARTESIAN_POINT ( 'NONE',  ( 0.000000000000000000, 0.000000000000000000, 47.00000000000000000 ) ) ;
#4766=TOROIDAL_SURFACE ( 'NONE', #1154, 6.500000000000000000, 1.000000000000000000 ) ;
#4784=EDGE_LOOP ( 'NONE', ( #1472, #5442 ) ) ;
#4793=( NAMED_UNIT ( * ) SI_UNIT ( $, .STERADIAN. ) SOLID_ANGLE_UNIT ( ) );
#4808=APPLICATION_CONTEXT ( 'automotive_design' ) ;
#4809=CARTESIAN_POINT ( 'NONE',  ( 0.000000000000000000, 0.000000000000000000, 1.000000000000000888 ) ) ;
#4817=CIRCLE ( 'NONE', #3790, 1.000000000000000000 ) ;
#4861=DIRECTION ( 'NONE',  ( -1.000000000000000000, 1.224646799147352468E-16, 0.000000000000000000 ) ) ;
#4871=EDGE_CURVE ( 'NONE', #5642, #6227, #1440, .T. ) ;
#4894=DIRECTION ( 'NONE',  ( 1.224646799147353207E-16, 1.000000000000000000, -0.000000000000000000 ) ) ;
#4901=( GEOMETRIC_REPRESENTATION_CONTEXT ( 3 ) GLOBAL_UNCERTAINTY_ASSIGNED_CONTEXT ( ( #5668 ) ) GLOBAL_UNIT_ASSIGNED_CONTEXT ( ( #3147, #714, #3660 ) ) REPRESENTATION_CONTEXT ( 'NONE', 'WORKASPACE' ) );
#4911=EDGE_LOOP ( 'NONE', ( #4296, #5209, #1271, #560 ) ) ;
#4932=VECTOR ( 'NONE', #962, 1000.000000000000000 ) ;
#4940=AXIS2_PLACEMENT_3D ( 'NONE', #6350, #105, #70 ) ;
#4962=DIRECTION ( 'NONE',  ( 1.000000000000000000, 0.000000000000000000, 0.000000000000000000 ) ) ;
#5014=CARTESIAN_POINT ( 'NONE',  ( 0.000000000000000000, 0.000000000000000000, 48.00000000000000000 ) ) ;
#5052=CARTESIAN_POINT ( 'NONE',  ( 0.000000000000000000, 0.000000000000000000, 1.000000000000000888 ) ) ;
#5064=EDGE_CURVE ( 'NONE', #371, #6227, #1025, .T. ) ;
#5074=DIRECTION ( 'NONE',  ( 1.000000000000000000, 0.000000000000000000, 0.000000000000000000 ) ) ;
#5088=PRODUCT_DEFINITION_SHAPE ( 'NONE', 'NONE',  #3336 ) ;
#5123=VECTOR ( 'NONE', #2062, 1000.000000000000000 ) ;
#5182=CARTESIAN_POINT ( 'NONE',  ( 7.500000000000000000, 9.184850993605147944E-16, 1.000000000000000888 ) ) ;
#5209=ORIENTED_EDGE ( 'NONE', *, *, #5748, .T. ) ;
#5219=DIRECTION ( 'NONE',  ( 0.000000000000000000, 0.000000000000000000, -1.000000000000000000 ) ) ;
#5226=APPLICATION_CONTEXT ( 'automotive_design' ) ;
#5267=CARTESIAN_POINT ( 'NONE',  ( -7.500000000000000000, 0.000000000000000000, 47.00000000000000000 ) ) ;
#5277=PLANE ( 'NONE',  #6256 ) ;
#5310=EDGE_CURVE ( 'NONE', #2368, #661, #3881, .T. ) ;
#5329=ORIENTED_EDGE ( 'NONE', *, *, #5986, .T. ) ;
#5353=AXIS2_PLACEMENT_3D ( 'NONE', #2558, #4520, #2079 ) ;
#5366=EDGE_LOOP ( 'NONE', ( #815, #1952, #213, #2258 ) ) ;
#5370=ADVANCED_FACE ( 'NONE', ( #2874 ), #5277, .T. ) ;
#5410=DIRECTION ( 'NONE',  ( -0.000000000000000000, -0.000000000000000000, -1.000000000000000000 ) ) ;
#5442=ORIENTED_EDGE ( 'NONE', *, *, #2499, .T. ) ;
#5445=PRODUCT_CONTEXT ( 'NONE', #5226, 'mechanical' ) ;
#5460=DIRECTION ( 'NONE',  ( 1.000000000000000000, 0.000000000000000000, -0.000000000000000000 ) ) ;
#5557=CIRCLE ( 'NONE', #4940, 6.500000000000000000 ) ;
#5586=CARTESIAN_POINT ( 'NONE',  ( 0.000000000000000000, 0.000000000000000000, 0.000000000000000000 ) ) ;
#5606=SHAPE_REPRESENTATION ( 'Part 32,6_Varsay\X2\0131\X0\lan', ( #6349 ), #1412 ) ;
#5642=VERTEX_POINT ( 'NONE', #5267 ) ;
#5649=VERTEX_POINT ( 'NONE', #787 ) ;
#5668=UNCERTAINTY_MEASURE_WITH_UNIT (LENGTH_MEASURE( 1.000000000000000082E-05 ), #3147, 'distance_accuracy_value', 'NONE');
#5681=ORIENTED_EDGE ( 'NONE', *, *, #4871, .T. ) ;
#5707=PRODUCT_DEFINITION_CONTEXT ( 'detailed design', #4808, 'design' ) ;
#5748=EDGE_CURVE ( 'NONE', #5642, #661, #3157, .T. ) ;
#5755=ORIENTED_EDGE ( 'NONE', *, *, #4072, .T. ) ;
#5773=CARTESIAN_POINT ( 'NONE',  ( 0.000000000000000000, 0.000000000000000000, 0.000000000000000000 ) ) ;
#5832=DIRECTION ( 'NONE',  ( 1.000000000000000000, 0.000000000000000000, 0.000000000000000000 ) ) ;
#5895=DIRECTION ( 'NONE',  ( 0.000000000000000000, 0.000000000000000000, -1.000000000000000000 ) ) ;
#5941=AXIS2_PLACEMENT_3D ( 'NONE', #5773, #1962, #1409 ) ;
#5986=EDGE_CURVE ( 'NONE', #1070, #371, #1639, .T. ) ;
#6015=CARTESIAN_POINT ( 'NONE',  ( -7.500000000000000000, 0.000000000000000000, 1.000000000000000888 ) ) ;
#6027=CARTESIAN_POINT ( 'NONE',  ( 6.500000000000000000, 0.000000000000000000, 47.00000000000000000 ) ) ;
#6031=EDGE_CURVE ( 'NONE', #1070, #2368, #4187, .T. ) ;
#6083=CYLINDRICAL_SURFACE ( 'NONE', #1813, 7.500000000000000000 ) ;
#6150=AXIS2_PLACEMENT_3D ( 'NONE', #6027, #1604, #5219 ) ;
#6227=VERTEX_POINT ( 'NONE', #6015 ) ;
#6237=AXIS2_PLACEMENT_3D ( 'NONE', #2059, #650, #1513 ) ;
#6247=EDGE_LOOP ( 'NONE', ( #4251, #854, #5681, #3980 ) ) ;
#6256=AXIS2_PLACEMENT_3D ( 'NONE', #3846, #3817, #6267 ) ;
#6259=AXIS2_PLACEMENT_3D ( 'NONE', #1291, #2254, #819 ) ;
#6267=DIRECTION ( 'NONE',  ( 1.000000000000000000, 0.000000000000000000, -0.000000000000000000 ) ) ;
#6285=AXIS2_PLACEMENT_3D ( 'NONE', #3983, #4894, #4861 ) ;
#6329=DIRECTION ( 'NONE',  ( 1.000000000000000000, 0.000000000000000000, 0.000000000000000000 ) ) ;
#6349=AXIS2_PLACEMENT_3D ( 'NONE', #290, #2242, #4169 ) ;
#6350=CARTESIAN_POINT ( 'NONE',  ( 0.000000000000000000, 0.000000000000000000, 48.00000000000000000 ) ) ;
#6413=COLOUR_RGB('Off White',0.89,0.88,0.83);
#6414=FILL_AREA_STYLE_COLOUR('',#6413);
#6415=FILL_AREA_STYLE('',(#6414));
#6416=SURFACE_STYLE_FILL_AREA(#6415);
#6417=SURFACE_SIDE_STYLE('',(#6416));
#6418=SURFACE_STYLE_USAGE(.BOTH.,#6417);
#6419=PRESENTATION_STYLE_ASSIGNMENT((#6418));
ENDSEC;
END-ISO-10303-21;
